ISO-10303-21;
HEADER;
/* Generated by software containing ST-Developer
 * from STEP Tools, Inc. (www.steptools.com) 
 */

FILE_DESCRIPTION(
/* description */ ('STEP AP214'),
/* implementation_level */ '2;1');

FILE_NAME(
/* name */ 'Ball Screw Shaft.step',
/* time_stamp */ '2026-11-15T14:49:54-08:00',
/* author */ (''),
/* organization */ (''),
/* preprocessor_version */ 'ST-DEVELOPER v20.2',
/* originating_system */ 'Autodesk Translation Framework v15.17.0.0',
/* authorisation */ '');

FILE_SCHEMA (('AUTOMOTIVE_DESIGN { 1 0 10303 214 3 1 1 }'));
ENDSEC;

DATA;
#10=MECHANICAL_DESIGN_GEOMETRIC_PRESENTATION_REPRESENTATION('',(#1107),#66721);
#70=TOROIDAL_SURFACE('',#27280,6.20000000000003,0.199999999999989);
#71=TOROIDAL_SURFACE('',#27288,7.7000000000001,0.199999999999989);
#72=TOROIDAL_SURFACE('',#27299,7.7,0.200000000000001);
#107=(
BOUNDED_CURVE()
B_SPLINE_CURVE(2,(#39908,#39909,#39910),.UNSPECIFIED.,.F.,.F.)
B_SPLINE_CURVE_WITH_KNOTS((3,3),(-0.517918190908586,-0.283395256102357),
 .UNSPECIFIED.)
CURVE()
GEOMETRIC_REPRESENTATION_ITEM()
RATIONAL_B_SPLINE_CURVE((1.11558191760503,1.10062774735407,1.07551718013297))
REPRESENTATION_ITEM('')
);
#108=(
BOUNDED_CURVE()
B_SPLINE_CURVE(2,(#39913,#39914,#39915),.UNSPECIFIED.,.F.,.F.)
B_SPLINE_CURVE_WITH_KNOTS((3,3),(-1.44305924653611,-1.2085363117164),
 .UNSPECIFIED.)
CURVE()
GEOMETRIC_REPRESENTATION_ITEM()
RATIONAL_B_SPLINE_CURVE((1.0755171801302,1.10062774735336,1.1155819176052))
REPRESENTATION_ITEM('')
);
#117=B_SPLINE_CURVE_WITH_KNOTS('',3,(#39818,#39819,#39820,#39821,#39822,
#39823,#39824,#39825,#39826,#39827,#39828,#39829,#39830,#39831,#39832,#39833,
#39834,#39835),.UNSPECIFIED.,.F.,.F.,(4,2,2,2,2,2,2,2,4),(0.607760117460578,
0.683747753705319,0.759735389950059,0.835687783070469,0.911640176190879,
0.987592569311288,1.0635449624317,1.13953259867644,1.21552023492118),
 .UNSPECIFIED.);
#541=CONICAL_SURFACE('',#27283,7.00000000000019,0.785398163397415);
#542=CONICAL_SURFACE('',#27291,9.00000000000005,0.785398163397447);
#543=CONICAL_SURFACE('',#27297,9.9999999999999,0.785398163397382);
#544=CONICAL_SURFACE('',#27312,7.5,0.785398163397448);
#545=CONICAL_SURFACE('',#27319,5.00000000000007,0.785398163397425);
#1045=SHAPE_REPRESENTATION_RELATIONSHIP('SRR','None',#66904,#1076);
#1076=ADVANCED_BREP_SHAPE_REPRESENTATION('',(#1142),#66695);
#1107=STYLED_ITEM('',(#67095),#1142);
#1142=MANIFOLD_SOLID_BREP('Body1',#25673);
#1302=FACE_BOUND('',#4471,.T.);
#1303=FACE_BOUND('',#4473,.T.);
#1304=FACE_BOUND('',#4475,.T.);
#1305=FACE_BOUND('',#4477,.T.);
#1306=FACE_BOUND('',#4479,.T.);
#1870=PLANE('',#27314);
#1871=PLANE('',#27315);
#1872=PLANE('',#27316);
#1873=PLANE('',#27317);
#1874=PLANE('',#27318);
#1875=PLANE('',#27321);
#1876=PLANE('',#27322);
#1877=PLANE('',#27323);
#1878=PLANE('',#27324);
#1879=PLANE('',#27325);
#2881=FACE_OUTER_BOUND('',#4457,.T.);
#2882=FACE_OUTER_BOUND('',#4458,.T.);
#2883=FACE_OUTER_BOUND('',#4459,.T.);
#2884=FACE_OUTER_BOUND('',#4460,.T.);
#2885=FACE_OUTER_BOUND('',#4461,.T.);
#2886=FACE_OUTER_BOUND('',#4462,.T.);
#2887=FACE_OUTER_BOUND('',#4463,.T.);
#2888=FACE_OUTER_BOUND('',#4464,.T.);
#2889=FACE_OUTER_BOUND('',#4465,.T.);
#2890=FACE_OUTER_BOUND('',#4466,.T.);
#2891=FACE_OUTER_BOUND('',#4467,.T.);
#2892=FACE_OUTER_BOUND('',#4468,.T.);
#2893=FACE_OUTER_BOUND('',#4469,.T.);
#2894=FACE_OUTER_BOUND('',#4470,.T.);
#2895=FACE_OUTER_BOUND('',#4472,.T.);
#2896=FACE_OUTER_BOUND('',#4474,.T.);
#2897=FACE_OUTER_BOUND('',#4476,.T.);
#2898=FACE_OUTER_BOUND('',#4478,.T.);
#2899=FACE_OUTER_BOUND('',#4480,.T.);
#2900=FACE_OUTER_BOUND('',#4481,.T.);
#2901=FACE_OUTER_BOUND('',#4482,.T.);
#2902=FACE_OUTER_BOUND('',#4483,.T.);
#2903=FACE_OUTER_BOUND('',#4484,.T.);
#2904=FACE_OUTER_BOUND('',#4485,.T.);
#2905=FACE_OUTER_BOUND('',#4486,.T.);
#4457=EDGE_LOOP('',(#19988,#19989,#19990,#19991,#19992,#19993,#19994,#19995));
#4458=EDGE_LOOP('',(#19996,#19997,#19998,#19999));
#4459=EDGE_LOOP('',(#20000,#20001,#20002,#20003));
#4460=EDGE_LOOP('',(#20004,#20005,#20006,#20007));
#4461=EDGE_LOOP('',(#20008,#20009,#20010,#20011));
#4462=EDGE_LOOP('',(#20012,#20013,#20014,#20015));
#4463=EDGE_LOOP('',(#20016,#20017,#20018,#20019,#20020));
#4464=EDGE_LOOP('',(#20021,#20022,#20023,#20024,#20025));
#4465=EDGE_LOOP('',(#20026,#20027,#20028,#20029));
#4466=EDGE_LOOP('',(#20030,#20031,#20032,#20033));
#4467=EDGE_LOOP('',(#20034,#20035,#20036,#20037));
#4468=EDGE_LOOP('',(#20038,#20039,#20040,#20041,#20042));
#4469=EDGE_LOOP('',(#20043,#20044,#20045,#20046,#20047));
#4470=EDGE_LOOP('',(#20048));
#4471=EDGE_LOOP('',(#20049));
#4472=EDGE_LOOP('',(#20050));
#4473=EDGE_LOOP('',(#20051));
#4474=EDGE_LOOP('',(#20052));
#4475=EDGE_LOOP('',(#20053));
#4476=EDGE_LOOP('',(#20054));
#4477=EDGE_LOOP('',(#20055));
#4478=EDGE_LOOP('',(#20056));
#4479=EDGE_LOOP('',(#20057));
#4480=EDGE_LOOP('',(#20058,#20059,#20060,#20061,#20062));
#4481=EDGE_LOOP('',(#20063,#20064,#20065,#20066));
#4482=EDGE_LOOP('',(#20067));
#4483=EDGE_LOOP('',(#20068,#20069,#20070,#20071,#20072));
#4484=EDGE_LOOP('',(#20073,#20074,#20075,#20076,#20077));
#4485=EDGE_LOOP('',(#20078,#20079,#20080,#20081));
#4486=EDGE_LOOP('',(#20082,#20083,#20084,#20085));
#6549=LINE('',#39812,#8538);
#6550=LINE('',#39816,#8539);
#6551=LINE('',#39837,#8540);
#6552=LINE('',#39847,#8541);
#6553=LINE('',#39852,#8542);
#6554=LINE('',#39861,#8543);
#6555=LINE('',#39868,#8544);
#6556=LINE('',#39871,#8545);
#6557=LINE('',#39882,#8546);
#6558=LINE('',#39887,#8547);
#6559=LINE('',#39895,#8548);
#6560=LINE('',#39899,#8549);
#6561=LINE('',#39918,#8550);
#6562=LINE('',#39920,#8551);
#6563=LINE('',#39921,#8552);
#6564=LINE('',#39925,#8553);
#6565=LINE('',#39926,#8554);
#6566=LINE('',#39929,#8555);
#6567=LINE('',#39930,#8556);
#8538=VECTOR('',#32296,6.00000000000003);
#8539=VECTOR('',#32299,1000.);
#8540=VECTOR('',#32300,1000.);
#8541=VECTOR('',#32313,7.00000000000019);
#8542=VECTOR('',#32320,7.5000000000001);
#8543=VECTOR('',#32331,9.00000000000005);
#8544=VECTOR('',#32340,9.99999999999998);
#8545=VECTOR('',#32343,9.9999999999999);
#8546=VECTOR('',#32358,7.5);
#8547=VECTOR('',#32363,7.15);
#8548=VECTOR('',#32372,7.5);
#8549=VECTOR('',#32377,7.5);
#8550=VECTOR('',#32396,1000.);
#8551=VECTOR('',#32397,1000.);
#8552=VECTOR('',#32398,1000.);
#8553=VECTOR('',#32403,1000.);
#8554=VECTOR('',#32404,1000.);
#8555=VECTOR('',#32407,1000.);
#8556=VECTOR('',#32408,1000.);
#9983=CIRCLE('',#27277,6.00000000000004);
#9984=CIRCLE('',#27278,6.00000000000002);
#9985=CIRCLE('',#27279,6.00000000000002);
#9986=CIRCLE('',#27281,6.20000000000003);
#9987=CIRCLE('',#27282,0.199999999999989);
#9988=CIRCLE('',#27284,7.5000000000001);
#9989=CIRCLE('',#27285,7.00000000000019);
#9990=CIRCLE('',#27287,7.50000000000011);
#9991=CIRCLE('',#27289,7.7000000000001);
#9992=CIRCLE('',#27290,0.199999999999989);
#9993=CIRCLE('',#27292,10.0000000000001);
#9994=CIRCLE('',#27293,9.00000000000005);
#9995=CIRCLE('',#27295,9.9999999999999);
#9996=CIRCLE('',#27296,9.9999999999999);
#9997=CIRCLE('',#27298,8.99999999999991);
#9998=CIRCLE('',#27300,7.5);
#9999=CIRCLE('',#27301,0.200000000000001);
#10000=CIRCLE('',#27302,7.7);
#10001=CIRCLE('',#27304,7.5);
#10002=CIRCLE('',#27306,7.15);
#10003=CIRCLE('',#27307,7.15);
#10004=CIRCLE('',#27309,7.5);
#10005=CIRCLE('',#27310,7.5);
#10006=CIRCLE('',#27311,7.5);
#10007=CIRCLE('',#27313,6.5);
#10008=CIRCLE('',#27320,5.00000000000007);
#10009=CIRCLE('',#27326,2.);
#11761=VERTEX_POINT('',#39809);
#11762=VERTEX_POINT('',#39811);
#11763=VERTEX_POINT('',#39813);
#11764=VERTEX_POINT('',#39815);
#11765=VERTEX_POINT('',#39817);
#11766=VERTEX_POINT('',#39836);
#11767=VERTEX_POINT('',#39840);
#11768=VERTEX_POINT('',#39844);
#11769=VERTEX_POINT('',#39846);
#11770=VERTEX_POINT('',#39850);
#11771=VERTEX_POINT('',#39854);
#11772=VERTEX_POINT('',#39858);
#11773=VERTEX_POINT('',#39860);
#11774=VERTEX_POINT('',#39864);
#11775=VERTEX_POINT('',#39865);
#11776=VERTEX_POINT('',#39870);
#11777=VERTEX_POINT('',#39874);
#11778=VERTEX_POINT('',#39876);
#11779=VERTEX_POINT('',#39880);
#11780=VERTEX_POINT('',#39884);
#11781=VERTEX_POINT('',#39886);
#11782=VERTEX_POINT('',#39890);
#11783=VERTEX_POINT('',#39891);
#11784=VERTEX_POINT('',#39894);
#11785=VERTEX_POINT('',#39898);
#11786=VERTEX_POINT('',#39907);
#11787=VERTEX_POINT('',#39911);
#11788=VERTEX_POINT('',#39917);
#11789=VERTEX_POINT('',#39919);
#11790=VERTEX_POINT('',#39924);
#11791=VERTEX_POINT('',#39928);
#14687=EDGE_CURVE('',#11761,#11761,#9983,.T.);
#14688=EDGE_CURVE('',#11761,#11762,#6549,.T.);
#14689=EDGE_CURVE('',#11762,#11763,#9984,.T.);
#14690=EDGE_CURVE('',#11763,#11764,#6550,.T.);
#14691=EDGE_CURVE('',#11764,#11765,#117,.F.);
#14692=EDGE_CURVE('',#11765,#11766,#6551,.T.);
#14693=EDGE_CURVE('',#11766,#11762,#9985,.T.);
#14694=EDGE_CURVE('',#11767,#11767,#9986,.T.);
#14695=EDGE_CURVE('',#11767,#11761,#9987,.T.);
#14696=EDGE_CURVE('',#11768,#11768,#9988,.T.);
#14697=EDGE_CURVE('',#11768,#11769,#6552,.T.);
#14698=EDGE_CURVE('',#11769,#11769,#9989,.T.);
#14699=EDGE_CURVE('',#11770,#11770,#9990,.T.);
#14700=EDGE_CURVE('',#11770,#11768,#6553,.T.);
#14701=EDGE_CURVE('',#11771,#11771,#9991,.T.);
#14702=EDGE_CURVE('',#11771,#11770,#9992,.T.);
#14703=EDGE_CURVE('',#11772,#11772,#9993,.T.);
#14704=EDGE_CURVE('',#11772,#11773,#6554,.T.);
#14705=EDGE_CURVE('',#11773,#11773,#9994,.T.);
#14706=EDGE_CURVE('',#11774,#11775,#9995,.T.);
#14707=EDGE_CURVE('',#11775,#11774,#9996,.T.);
#14708=EDGE_CURVE('',#11775,#11772,#6555,.T.);
#14709=EDGE_CURVE('',#11774,#11776,#6556,.T.);
#14710=EDGE_CURVE('',#11776,#11776,#9997,.T.);
#14711=EDGE_CURVE('',#11777,#11777,#9998,.T.);
#14712=EDGE_CURVE('',#11777,#11778,#9999,.T.);
#14713=EDGE_CURVE('',#11778,#11778,#10000,.T.);
#14714=EDGE_CURVE('',#11779,#11779,#10001,.T.);
#14715=EDGE_CURVE('',#11779,#11777,#6557,.T.);
#14716=EDGE_CURVE('',#11780,#11780,#10002,.T.);
#14717=EDGE_CURVE('',#11780,#11781,#6558,.T.);
#14718=EDGE_CURVE('',#11781,#11781,#10003,.T.);
#14719=EDGE_CURVE('',#11782,#11783,#10004,.T.);
#14720=EDGE_CURVE('',#11783,#11782,#10005,.T.);
#14721=EDGE_CURVE('',#11783,#11784,#6559,.T.);
#14722=EDGE_CURVE('',#11784,#11784,#10006,.T.);
#14723=EDGE_CURVE('',#11782,#11785,#6560,.T.);
#14724=EDGE_CURVE('',#11785,#11785,#10007,.T.);
#14725=EDGE_CURVE('',#11766,#11786,#107,.T.);
#14726=EDGE_CURVE('',#11786,#11787,#10008,.T.);
#14727=EDGE_CURVE('',#11787,#11763,#108,.T.);
#14728=EDGE_CURVE('',#11788,#11786,#6561,.T.);
#14729=EDGE_CURVE('',#11789,#11788,#6562,.T.);
#14730=EDGE_CURVE('',#11789,#11787,#6563,.T.);
#14731=EDGE_CURVE('',#11765,#11790,#6564,.T.);
#14732=EDGE_CURVE('',#11790,#11788,#6565,.T.);
#14733=EDGE_CURVE('',#11791,#11789,#6566,.T.);
#14734=EDGE_CURVE('',#11791,#11764,#6567,.T.);
#14735=EDGE_CURVE('',#11790,#11791,#10009,.T.);
#19988=ORIENTED_EDGE('',*,*,#14687,.F.);
#19989=ORIENTED_EDGE('',*,*,#14688,.T.);
#19990=ORIENTED_EDGE('',*,*,#14689,.T.);
#19991=ORIENTED_EDGE('',*,*,#14690,.T.);
#19992=ORIENTED_EDGE('',*,*,#14691,.T.);
#19993=ORIENTED_EDGE('',*,*,#14692,.T.);
#19994=ORIENTED_EDGE('',*,*,#14693,.T.);
#19995=ORIENTED_EDGE('',*,*,#14688,.F.);
#19996=ORIENTED_EDGE('',*,*,#14694,.F.);
#19997=ORIENTED_EDGE('',*,*,#14695,.T.);
#19998=ORIENTED_EDGE('',*,*,#14687,.T.);
#19999=ORIENTED_EDGE('',*,*,#14695,.F.);
#20000=ORIENTED_EDGE('',*,*,#14696,.F.);
#20001=ORIENTED_EDGE('',*,*,#14697,.T.);
#20002=ORIENTED_EDGE('',*,*,#14698,.T.);
#20003=ORIENTED_EDGE('',*,*,#14697,.F.);
#20004=ORIENTED_EDGE('',*,*,#14699,.F.);
#20005=ORIENTED_EDGE('',*,*,#14700,.T.);
#20006=ORIENTED_EDGE('',*,*,#14696,.T.);
#20007=ORIENTED_EDGE('',*,*,#14700,.F.);
#20008=ORIENTED_EDGE('',*,*,#14701,.F.);
#20009=ORIENTED_EDGE('',*,*,#14702,.T.);
#20010=ORIENTED_EDGE('',*,*,#14699,.T.);
#20011=ORIENTED_EDGE('',*,*,#14702,.F.);
#20012=ORIENTED_EDGE('',*,*,#14703,.F.);
#20013=ORIENTED_EDGE('',*,*,#14704,.T.);
#20014=ORIENTED_EDGE('',*,*,#14705,.T.);
#20015=ORIENTED_EDGE('',*,*,#14704,.F.);
#20016=ORIENTED_EDGE('',*,*,#14706,.F.);
#20017=ORIENTED_EDGE('',*,*,#14707,.F.);
#20018=ORIENTED_EDGE('',*,*,#14708,.T.);
#20019=ORIENTED_EDGE('',*,*,#14703,.T.);
#20020=ORIENTED_EDGE('',*,*,#14708,.F.);
#20021=ORIENTED_EDGE('',*,*,#14706,.T.);
#20022=ORIENTED_EDGE('',*,*,#14707,.T.);
#20023=ORIENTED_EDGE('',*,*,#14709,.T.);
#20024=ORIENTED_EDGE('',*,*,#14710,.F.);
#20025=ORIENTED_EDGE('',*,*,#14709,.F.);
#20026=ORIENTED_EDGE('',*,*,#14711,.F.);
#20027=ORIENTED_EDGE('',*,*,#14712,.T.);
#20028=ORIENTED_EDGE('',*,*,#14713,.T.);
#20029=ORIENTED_EDGE('',*,*,#14712,.F.);
#20030=ORIENTED_EDGE('',*,*,#14714,.F.);
#20031=ORIENTED_EDGE('',*,*,#14715,.T.);
#20032=ORIENTED_EDGE('',*,*,#14711,.T.);
#20033=ORIENTED_EDGE('',*,*,#14715,.F.);
#20034=ORIENTED_EDGE('',*,*,#14716,.F.);
#20035=ORIENTED_EDGE('',*,*,#14717,.T.);
#20036=ORIENTED_EDGE('',*,*,#14718,.T.);
#20037=ORIENTED_EDGE('',*,*,#14717,.F.);
#20038=ORIENTED_EDGE('',*,*,#14719,.F.);
#20039=ORIENTED_EDGE('',*,*,#14720,.F.);
#20040=ORIENTED_EDGE('',*,*,#14721,.T.);
#20041=ORIENTED_EDGE('',*,*,#14722,.T.);
#20042=ORIENTED_EDGE('',*,*,#14721,.F.);
#20043=ORIENTED_EDGE('',*,*,#14719,.T.);
#20044=ORIENTED_EDGE('',*,*,#14720,.T.);
#20045=ORIENTED_EDGE('',*,*,#14723,.T.);
#20046=ORIENTED_EDGE('',*,*,#14724,.F.);
#20047=ORIENTED_EDGE('',*,*,#14723,.F.);
#20048=ORIENTED_EDGE('',*,*,#14722,.F.);
#20049=ORIENTED_EDGE('',*,*,#14716,.T.);
#20050=ORIENTED_EDGE('',*,*,#14714,.T.);
#20051=ORIENTED_EDGE('',*,*,#14718,.F.);
#20052=ORIENTED_EDGE('',*,*,#14710,.T.);
#20053=ORIENTED_EDGE('',*,*,#14713,.F.);
#20054=ORIENTED_EDGE('',*,*,#14705,.F.);
#20055=ORIENTED_EDGE('',*,*,#14701,.T.);
#20056=ORIENTED_EDGE('',*,*,#14698,.F.);
#20057=ORIENTED_EDGE('',*,*,#14694,.T.);
#20058=ORIENTED_EDGE('',*,*,#14693,.F.);
#20059=ORIENTED_EDGE('',*,*,#14725,.T.);
#20060=ORIENTED_EDGE('',*,*,#14726,.T.);
#20061=ORIENTED_EDGE('',*,*,#14727,.T.);
#20062=ORIENTED_EDGE('',*,*,#14689,.F.);
#20063=ORIENTED_EDGE('',*,*,#14726,.F.);
#20064=ORIENTED_EDGE('',*,*,#14728,.F.);
#20065=ORIENTED_EDGE('',*,*,#14729,.F.);
#20066=ORIENTED_EDGE('',*,*,#14730,.T.);
#20067=ORIENTED_EDGE('',*,*,#14724,.T.);
#20068=ORIENTED_EDGE('',*,*,#14692,.F.);
#20069=ORIENTED_EDGE('',*,*,#14731,.T.);
#20070=ORIENTED_EDGE('',*,*,#14732,.T.);
#20071=ORIENTED_EDGE('',*,*,#14728,.T.);
#20072=ORIENTED_EDGE('',*,*,#14725,.F.);
#20073=ORIENTED_EDGE('',*,*,#14733,.F.);
#20074=ORIENTED_EDGE('',*,*,#14734,.T.);
#20075=ORIENTED_EDGE('',*,*,#14690,.F.);
#20076=ORIENTED_EDGE('',*,*,#14727,.F.);
#20077=ORIENTED_EDGE('',*,*,#14730,.F.);
#20078=ORIENTED_EDGE('',*,*,#14735,.T.);
#20079=ORIENTED_EDGE('',*,*,#14733,.T.);
#20080=ORIENTED_EDGE('',*,*,#14729,.T.);
#20081=ORIENTED_EDGE('',*,*,#14732,.F.);
#20082=ORIENTED_EDGE('',*,*,#14731,.F.);
#20083=ORIENTED_EDGE('',*,*,#14691,.F.);
#20084=ORIENTED_EDGE('',*,*,#14734,.F.);
#20085=ORIENTED_EDGE('',*,*,#14735,.F.);
#24020=CYLINDRICAL_SURFACE('',#27276,6.00000000000003);
#24021=CYLINDRICAL_SURFACE('',#27286,7.5000000000001);
#24022=CYLINDRICAL_SURFACE('',#27294,9.99999999999998);
#24023=CYLINDRICAL_SURFACE('',#27303,7.5);
#24024=CYLINDRICAL_SURFACE('',#27305,7.15);
#24025=CYLINDRICAL_SURFACE('',#27308,7.5);
#24026=CYLINDRICAL_SURFACE('',#27327,2.);
#24834=ADVANCED_FACE('',(#2881),#24020,.T.);
#24835=ADVANCED_FACE('',(#2882),#70,.F.);
#24836=ADVANCED_FACE('',(#2883),#541,.T.);
#24837=ADVANCED_FACE('',(#2884),#24021,.T.);
#24838=ADVANCED_FACE('',(#2885),#71,.F.);
#24839=ADVANCED_FACE('',(#2886),#542,.T.);
#24840=ADVANCED_FACE('',(#2887),#24022,.T.);
#24841=ADVANCED_FACE('',(#2888),#543,.T.);
#24842=ADVANCED_FACE('',(#2889),#72,.F.);
#24843=ADVANCED_FACE('',(#2890),#24023,.T.);
#24844=ADVANCED_FACE('',(#2891),#24024,.T.);
#24845=ADVANCED_FACE('',(#2892),#24025,.T.);
#24846=ADVANCED_FACE('',(#2893),#544,.T.);
#24847=ADVANCED_FACE('',(#2894,#1302),#1870,.F.);
#24848=ADVANCED_FACE('',(#2895,#1303),#1871,.F.);
#24849=ADVANCED_FACE('',(#2896,#1304),#1872,.F.);
#24850=ADVANCED_FACE('',(#2897,#1305),#1873,.F.);
#24851=ADVANCED_FACE('',(#2898,#1306),#1874,.F.);
#24852=ADVANCED_FACE('',(#2899),#545,.T.);
#24853=ADVANCED_FACE('',(#2900),#1875,.F.);
#24854=ADVANCED_FACE('',(#2901),#1876,.F.);
#24855=ADVANCED_FACE('',(#2902),#1877,.F.);
#24856=ADVANCED_FACE('',(#2903),#1878,.F.);
#24857=ADVANCED_FACE('',(#2904),#1879,.F.);
#24858=ADVANCED_FACE('',(#2905),#24026,.F.);
#25673=CLOSED_SHELL('',(#24834,#24835,#24836,#24837,#24838,#24839,#24840,
#24841,#24842,#24843,#24844,#24845,#24846,#24847,#24848,#24849,#24850,#24851,
#24852,#24853,#24854,#24855,#24856,#24857,#24858));
#27275=AXIS2_PLACEMENT_3D('',#39807,#32290,#32291);
#27276=AXIS2_PLACEMENT_3D('',#39808,#32292,#32293);
#27277=AXIS2_PLACEMENT_3D('',#39810,#32294,#32295);
#27278=AXIS2_PLACEMENT_3D('',#39814,#32297,#32298);
#27279=AXIS2_PLACEMENT_3D('',#39838,#32301,#32302);
#27280=AXIS2_PLACEMENT_3D('',#39839,#32303,#32304);
#27281=AXIS2_PLACEMENT_3D('',#39841,#32305,#32306);
#27282=AXIS2_PLACEMENT_3D('',#39842,#32307,#32308);
#27283=AXIS2_PLACEMENT_3D('',#39843,#32309,#32310);
#27284=AXIS2_PLACEMENT_3D('',#39845,#32311,#32312);
#27285=AXIS2_PLACEMENT_3D('',#39848,#32314,#32315);
#27286=AXIS2_PLACEMENT_3D('',#39849,#32316,#32317);
#27287=AXIS2_PLACEMENT_3D('',#39851,#32318,#32319);
#27288=AXIS2_PLACEMENT_3D('',#39853,#32321,#32322);
#27289=AXIS2_PLACEMENT_3D('',#39855,#32323,#32324);
#27290=AXIS2_PLACEMENT_3D('',#39856,#32325,#32326);
#27291=AXIS2_PLACEMENT_3D('',#39857,#32327,#32328);
#27292=AXIS2_PLACEMENT_3D('',#39859,#32329,#32330);
#27293=AXIS2_PLACEMENT_3D('',#39862,#32332,#32333);
#27294=AXIS2_PLACEMENT_3D('',#39863,#32334,#32335);
#27295=AXIS2_PLACEMENT_3D('',#39866,#32336,#32337);
#27296=AXIS2_PLACEMENT_3D('',#39867,#32338,#32339);
#27297=AXIS2_PLACEMENT_3D('',#39869,#32341,#32342);
#27298=AXIS2_PLACEMENT_3D('',#39872,#32344,#32345);
#27299=AXIS2_PLACEMENT_3D('',#39873,#32346,#32347);
#27300=AXIS2_PLACEMENT_3D('',#39875,#32348,#32349);
#27301=AXIS2_PLACEMENT_3D('',#39877,#32350,#32351);
#27302=AXIS2_PLACEMENT_3D('',#39878,#32352,#32353);
#27303=AXIS2_PLACEMENT_3D('',#39879,#32354,#32355);
#27304=AXIS2_PLACEMENT_3D('',#39881,#32356,#32357);
#27305=AXIS2_PLACEMENT_3D('',#39883,#32359,#32360);
#27306=AXIS2_PLACEMENT_3D('',#39885,#32361,#32362);
#27307=AXIS2_PLACEMENT_3D('',#39888,#32364,#32365);
#27308=AXIS2_PLACEMENT_3D('',#39889,#32366,#32367);
#27309=AXIS2_PLACEMENT_3D('',#39892,#32368,#32369);
#27310=AXIS2_PLACEMENT_3D('',#39893,#32370,#32371);
#27311=AXIS2_PLACEMENT_3D('',#39896,#32373,#32374);
#27312=AXIS2_PLACEMENT_3D('',#39897,#32375,#32376);
#27313=AXIS2_PLACEMENT_3D('',#39900,#32378,#32379);
#27314=AXIS2_PLACEMENT_3D('',#39901,#32380,#32381);
#27315=AXIS2_PLACEMENT_3D('',#39902,#32382,#32383);
#27316=AXIS2_PLACEMENT_3D('',#39903,#32384,#32385);
#27317=AXIS2_PLACEMENT_3D('',#39904,#32386,#32387);
#27318=AXIS2_PLACEMENT_3D('',#39905,#32388,#32389);
#27319=AXIS2_PLACEMENT_3D('',#39906,#32390,#32391);
#27320=AXIS2_PLACEMENT_3D('',#39912,#32392,#32393);
#27321=AXIS2_PLACEMENT_3D('',#39916,#32394,#32395);
#27322=AXIS2_PLACEMENT_3D('',#39922,#32399,#32400);
#27323=AXIS2_PLACEMENT_3D('',#39923,#32401,#32402);
#27324=AXIS2_PLACEMENT_3D('',#39927,#32405,#32406);
#27325=AXIS2_PLACEMENT_3D('',#39931,#32409,#32410);
#27326=AXIS2_PLACEMENT_3D('',#39932,#32411,#32412);
#27327=AXIS2_PLACEMENT_3D('',#39933,#32413,#32414);
#32290=DIRECTION('axis',(0.,0.,1.));
#32291=DIRECTION('refdir',(1.,0.,0.));
#32292=DIRECTION('center_axis',(-1.,0.,0.));
#32293=DIRECTION('ref_axis',(0.,0.,1.));
#32294=DIRECTION('center_axis',(-1.,0.,0.));
#32295=DIRECTION('ref_axis',(0.,0.,1.));
#32296=DIRECTION('',(1.,0.,0.));
#32297=DIRECTION('center_axis',(-1.,0.,0.));
#32298=DIRECTION('ref_axis',(0.,0.,1.));
#32299=DIRECTION('',(-1.,0.,0.));
#32300=DIRECTION('',(1.,0.,0.));
#32301=DIRECTION('center_axis',(-1.,0.,0.));
#32302=DIRECTION('ref_axis',(0.,0.,1.));
#32303=DIRECTION('center_axis',(-1.,0.,0.));
#32304=DIRECTION('ref_axis',(0.,0.,1.));
#32305=DIRECTION('center_axis',(-1.,0.,0.));
#32306=DIRECTION('ref_axis',(0.,0.,1.));
#32307=DIRECTION('center_axis',(0.,1.,-1.22464679914735E-16));
#32308=DIRECTION('ref_axis',(0.,-1.22464679914735E-16,-1.));
#32309=DIRECTION('center_axis',(-1.,0.,0.));
#32310=DIRECTION('ref_axis',(0.,0.,1.));
#32311=DIRECTION('center_axis',(-1.,0.,0.));
#32312=DIRECTION('ref_axis',(0.,0.,1.));
#32313=DIRECTION('',(0.707106781186571,8.65956056235465E-17,0.707106781186524));
#32314=DIRECTION('center_axis',(-1.,0.,0.));
#32315=DIRECTION('ref_axis',(0.,0.,1.));
#32316=DIRECTION('center_axis',(-1.,0.,0.));
#32317=DIRECTION('ref_axis',(0.,0.,1.));
#32318=DIRECTION('center_axis',(-1.,0.,0.));
#32319=DIRECTION('ref_axis',(0.,0.,1.));
#32320=DIRECTION('',(1.,0.,0.));
#32321=DIRECTION('center_axis',(-1.,0.,0.));
#32322=DIRECTION('ref_axis',(0.,0.,1.));
#32323=DIRECTION('center_axis',(-1.,0.,0.));
#32324=DIRECTION('ref_axis',(0.,0.,1.));
#32325=DIRECTION('center_axis',(0.,1.,-1.22464679914735E-16));
#32326=DIRECTION('ref_axis',(0.,-1.22464679914735E-16,-1.));
#32327=DIRECTION('center_axis',(-1.,0.,0.));
#32328=DIRECTION('ref_axis',(0.,0.,1.));
#32329=DIRECTION('center_axis',(-1.,0.,0.));
#32330=DIRECTION('ref_axis',(0.,0.,1.));
#32331=DIRECTION('',(0.707106781186548,8.65956056235492E-17,0.707106781186547));
#32332=DIRECTION('center_axis',(-1.,0.,0.));
#32333=DIRECTION('ref_axis',(0.,0.,1.));
#32334=DIRECTION('center_axis',(-1.,0.,0.));
#32335=DIRECTION('ref_axis',(0.,0.,1.));
#32336=DIRECTION('center_axis',(-1.,0.,0.));
#32337=DIRECTION('ref_axis',(0.,0.,1.));
#32338=DIRECTION('center_axis',(-1.,0.,0.));
#32339=DIRECTION('ref_axis',(0.,0.,1.));
#32340=DIRECTION('',(1.,0.,0.));
#32341=DIRECTION('center_axis',(1.,0.,0.));
#32342=DIRECTION('ref_axis',(0.,0.,-1.));
#32343=DIRECTION('',(-0.707106781186594,8.65956056235436E-17,-0.707106781186501));
#32344=DIRECTION('center_axis',(-1.,0.,0.));
#32345=DIRECTION('ref_axis',(0.,0.,1.));
#32346=DIRECTION('center_axis',(-1.,0.,0.));
#32347=DIRECTION('ref_axis',(0.,0.,1.));
#32348=DIRECTION('center_axis',(-1.,0.,0.));
#32349=DIRECTION('ref_axis',(0.,0.,1.));
#32350=DIRECTION('center_axis',(0.,1.,-1.22464679914735E-16));
#32351=DIRECTION('ref_axis',(0.,-1.22464679914735E-16,-1.));
#32352=DIRECTION('center_axis',(-1.,0.,0.));
#32353=DIRECTION('ref_axis',(0.,0.,1.));
#32354=DIRECTION('center_axis',(-1.,0.,0.));
#32355=DIRECTION('ref_axis',(0.,0.,1.));
#32356=DIRECTION('center_axis',(-1.,0.,0.));
#32357=DIRECTION('ref_axis',(0.,0.,1.));
#32358=DIRECTION('',(1.,0.,0.));
#32359=DIRECTION('center_axis',(-1.,0.,0.));
#32360=DIRECTION('ref_axis',(0.,0.,1.));
#32361=DIRECTION('center_axis',(-1.,0.,0.));
#32362=DIRECTION('ref_axis',(0.,0.,1.));
#32363=DIRECTION('',(1.,0.,0.));
#32364=DIRECTION('center_axis',(-1.,0.,0.));
#32365=DIRECTION('ref_axis',(0.,0.,1.));
#32366=DIRECTION('center_axis',(-1.,0.,0.));
#32367=DIRECTION('ref_axis',(0.,0.,1.));
#32368=DIRECTION('center_axis',(-1.,0.,0.));
#32369=DIRECTION('ref_axis',(0.,0.,1.));
#32370=DIRECTION('center_axis',(-1.,0.,0.));
#32371=DIRECTION('ref_axis',(0.,0.,1.));
#32372=DIRECTION('',(1.,0.,0.));
#32373=DIRECTION('center_axis',(-1.,0.,0.));
#32374=DIRECTION('ref_axis',(0.,0.,1.));
#32375=DIRECTION('center_axis',(1.,0.,0.));
#32376=DIRECTION('ref_axis',(0.,0.,-1.));
#32377=DIRECTION('',(-0.707106781186547,8.65956056235493E-17,-0.707106781186547));
#32378=DIRECTION('center_axis',(-1.,0.,0.));
#32379=DIRECTION('ref_axis',(0.,0.,1.));
#32380=DIRECTION('center_axis',(-1.,0.,0.));
#32381=DIRECTION('ref_axis',(0.,0.,1.));
#32382=DIRECTION('center_axis',(1.,0.,0.));
#32383=DIRECTION('ref_axis',(0.,0.,-1.));
#32384=DIRECTION('center_axis',(1.,0.,0.));
#32385=DIRECTION('ref_axis',(0.,0.,-1.));
#32386=DIRECTION('center_axis',(-1.,0.,0.));
#32387=DIRECTION('ref_axis',(0.,0.,1.));
#32388=DIRECTION('center_axis',(-1.,0.,0.));
#32389=DIRECTION('ref_axis',(0.,0.,1.));
#32390=DIRECTION('center_axis',(-1.,0.,0.));
#32391=DIRECTION('ref_axis',(0.,-3.21624529935327E-16,-1.));
#32392=DIRECTION('center_axis',(-1.,0.,0.));
#32393=DIRECTION('ref_axis',(0.,0.,1.));
#32394=DIRECTION('center_axis',(-1.,0.,0.));
#32395=DIRECTION('ref_axis',(0.,0.,1.));
#32396=DIRECTION('',(0.,1.73472347597681E-16,1.));
#32397=DIRECTION('',(0.,1.,-2.16840434497101E-16));
#32398=DIRECTION('',(0.,-3.46944695195362E-16,1.));
#32399=DIRECTION('center_axis',(1.,0.,0.));
#32400=DIRECTION('ref_axis',(0.,0.,-1.));
#32401=DIRECTION('center_axis',(0.,1.,-1.73472347597681E-16));
#32402=DIRECTION('ref_axis',(0.,1.73472347597681E-16,1.));
#32403=DIRECTION('',(0.,-1.73472347597681E-16,-1.));
#32404=DIRECTION('',(1.,0.,0.));
#32405=DIRECTION('center_axis',(0.,-1.,-3.46944695195362E-16));
#32406=DIRECTION('ref_axis',(0.,3.46944695195362E-16,-1.));
#32407=DIRECTION('',(1.,0.,0.));
#32408=DIRECTION('',(0.,-3.46944695195362E-16,1.));
#32409=DIRECTION('center_axis',(0.,-2.16840434497101E-16,-1.));
#32410=DIRECTION('ref_axis',(0.,1.,-2.16840434497101E-16));
#32411=DIRECTION('center_axis',(0.,2.16840434497101E-16,1.));
#32412=DIRECTION('ref_axis',(0.,1.,-2.16840434497101E-16));
#32413=DIRECTION('center_axis',(0.,-1.73472347597681E-16,-1.));
#32414=DIRECTION('ref_axis',(0.,1.,-1.73472347597681E-16));
#39807=CARTESIAN_POINT('',(0.,0.,0.));
#39808=CARTESIAN_POINT('Origin',(-10.,0.,0.));
#39809=CARTESIAN_POINT('',(830.2,-7.34788079488416E-16,-6.00000000000003));
#39810=CARTESIAN_POINT('Origin',(830.2,0.,0.));
#39811=CARTESIAN_POINT('',(849.,-7.34788079488416E-16,-6.00000000000003));
#39812=CARTESIAN_POINT('',(-10.,-7.34788079488416E-16,-6.00000000000003));
#39813=CARTESIAN_POINT('',(849.,-2.,5.65685424949241));
#39814=CARTESIAN_POINT('Origin',(849.,0.,0.));
#39815=CARTESIAN_POINT('',(840.,-2.,5.65685424949241));
#39816=CARTESIAN_POINT('',(-10.,-2.,5.65685424949241));
#39817=CARTESIAN_POINT('',(840.,2.,5.65685424949241));
#39818=CARTESIAN_POINT('Ctrl Pts',(840.,2.,5.65685424949241));
#39819=CARTESIAN_POINT('Ctrl Pts',(839.746707879184,2.,5.65685424949241));
#39820=CARTESIAN_POINT('Ctrl Pts',(839.477996053073,1.94898067853764,5.67565356574254));
#39821=CARTESIAN_POINT('Ctrl Pts',(838.985893640085,1.74430581525273,5.74186082552468));
#39822=CARTESIAN_POINT('Ctrl Pts',(838.762313835253,1.59074095999942,5.788137712126));
#39823=CARTESIAN_POINT('Ctrl Pts',(838.409340913544,1.23776803829002,5.87374622031368));
#39824=CARTESIAN_POINT('Ctrl Pts',(838.255713027767,1.01415562391481,5.91887391060683));
#39825=CARTESIAN_POINT('Ctrl Pts',(838.050991158394,0.521932274441699,5.98240475886915));
#39826=CARTESIAN_POINT('Ctrl Pts',(838.,0.253174643734701,6.00000000000003));
#39827=CARTESIAN_POINT('Ctrl Pts',(838.,-0.253174643734697,6.00000000000003));
#39828=CARTESIAN_POINT('Ctrl Pts',(838.050991158394,-0.521932274441696,
5.98240475886915));
#39829=CARTESIAN_POINT('Ctrl Pts',(838.255713027767,-1.0141556239148,5.91887391060683));
#39830=CARTESIAN_POINT('Ctrl Pts',(838.409340913544,-1.23776803829001,5.87374622031368));
#39831=CARTESIAN_POINT('Ctrl Pts',(838.762313835253,-1.59074095999941,5.788137712126));
#39832=CARTESIAN_POINT('Ctrl Pts',(838.985893640085,-1.74430581525273,5.74186082552468));
#39833=CARTESIAN_POINT('Ctrl Pts',(839.477996053073,-1.94898067853763,5.67565356574254));
#39834=CARTESIAN_POINT('Ctrl Pts',(839.746707879184,-2.,5.65685424949241));
#39835=CARTESIAN_POINT('Ctrl Pts',(840.,-2.,5.65685424949241));
#39836=CARTESIAN_POINT('',(849.,2.,5.65685424949241));
#39837=CARTESIAN_POINT('',(-10.,2.,5.65685424949241));
#39838=CARTESIAN_POINT('Origin',(849.,0.,0.));
#39839=CARTESIAN_POINT('Origin',(830.2,0.,0.));
#39840=CARTESIAN_POINT('',(830.,-7.59281015471362E-16,-6.20000000000003));
#39841=CARTESIAN_POINT('Origin',(830.,0.,0.));
#39842=CARTESIAN_POINT('Origin',(830.2,-7.59281015471362E-16,-6.20000000000003));
#39843=CARTESIAN_POINT('Origin',(830.,0.,0.));
#39844=CARTESIAN_POINT('',(829.5,-9.18485099360529E-16,-7.50000000000011));
#39845=CARTESIAN_POINT('Origin',(829.5,0.,0.));
#39846=CARTESIAN_POINT('',(830.,-8.5725275940317E-16,-7.00000000000019));
#39847=CARTESIAN_POINT('',(830.,-8.5725275940317E-16,-7.00000000000019));
#39848=CARTESIAN_POINT('Origin',(830.,0.,0.));
#39849=CARTESIAN_POINT('Origin',(-10.,0.,0.));
#39850=CARTESIAN_POINT('',(790.2,-9.18485099360528E-16,-7.5000000000001));
#39851=CARTESIAN_POINT('Origin',(790.2,0.,0.));
#39852=CARTESIAN_POINT('',(-10.,-9.18485099360528E-16,-7.5000000000001));
#39853=CARTESIAN_POINT('Origin',(790.2,0.,0.));
#39854=CARTESIAN_POINT('',(790.,-9.42978035343474E-16,-7.7000000000001));
#39855=CARTESIAN_POINT('Origin',(790.,0.,0.));
#39856=CARTESIAN_POINT('Origin',(790.2,-9.42978035343474E-16,-7.7000000000001));
#39857=CARTESIAN_POINT('Origin',(790.,0.,0.));
#39858=CARTESIAN_POINT('',(789.,-1.22464679914736E-15,-10.0000000000001));
#39859=CARTESIAN_POINT('Origin',(789.,0.,0.));
#39860=CARTESIAN_POINT('',(790.,-1.10218211923262E-15,-9.00000000000005));
#39861=CARTESIAN_POINT('',(790.,-1.10218211923262E-15,-9.00000000000005));
#39862=CARTESIAN_POINT('Origin',(790.,0.,0.));
#39863=CARTESIAN_POINT('Origin',(-10.,0.,0.));
#39864=CARTESIAN_POINT('',(14.,1.22464679914734E-15,9.9999999999999));
#39865=CARTESIAN_POINT('',(14.,-1.22464679914735E-15,-9.99999999999998));
#39866=CARTESIAN_POINT('Origin',(14.,0.,0.));
#39867=CARTESIAN_POINT('Origin',(14.,0.,0.));
#39868=CARTESIAN_POINT('',(-10.,-1.22464679914735E-15,-9.99999999999998));
#39869=CARTESIAN_POINT('Origin',(14.,0.,0.));
#39870=CARTESIAN_POINT('',(12.9999999999999,-1.10218211923261E-15,8.99999999999991));
#39871=CARTESIAN_POINT('',(14.,-1.22464679914734E-15,9.9999999999999));
#39872=CARTESIAN_POINT('Origin',(12.9999999999999,0.,0.));
#39873=CARTESIAN_POINT('Origin',(12.8,0.,0.));
#39874=CARTESIAN_POINT('',(12.8,-9.18485099360515E-16,-7.5));
#39875=CARTESIAN_POINT('Origin',(12.8,0.,0.));
#39876=CARTESIAN_POINT('',(13.,-9.42978035343462E-16,-7.7));
#39877=CARTESIAN_POINT('Origin',(12.8,-9.42978035343462E-16,-7.7));
#39878=CARTESIAN_POINT('Origin',(13.,0.,0.));
#39879=CARTESIAN_POINT('Origin',(-10.,0.,0.));
#39880=CARTESIAN_POINT('',(4.00000000000001,-9.18485099360515E-16,-7.5));
#39881=CARTESIAN_POINT('Origin',(4.00000000000001,0.,0.));
#39882=CARTESIAN_POINT('',(-10.,-9.18485099360515E-16,-7.5));
#39883=CARTESIAN_POINT('Origin',(-10.,0.,0.));
#39884=CARTESIAN_POINT('',(2.85000000000001,-8.75622461390357E-16,-7.15));
#39885=CARTESIAN_POINT('Origin',(2.85000000000001,0.,0.));
#39886=CARTESIAN_POINT('',(4.00000000000001,-8.75622461390357E-16,-7.15));
#39887=CARTESIAN_POINT('',(-10.,-8.75622461390357E-16,-7.15));
#39888=CARTESIAN_POINT('Origin',(4.00000000000001,0.,0.));
#39889=CARTESIAN_POINT('Origin',(-10.,0.,0.));
#39890=CARTESIAN_POINT('',(1.,9.18485099360515E-16,7.5));
#39891=CARTESIAN_POINT('',(1.,-9.18485099360515E-16,-7.5));
#39892=CARTESIAN_POINT('Origin',(1.,0.,0.));
#39893=CARTESIAN_POINT('Origin',(1.,0.,0.));
#39894=CARTESIAN_POINT('',(2.85000000000001,-9.18485099360515E-16,-7.5));
#39895=CARTESIAN_POINT('',(-10.,-9.18485099360515E-16,-7.5));
#39896=CARTESIAN_POINT('Origin',(2.85000000000001,0.,0.));
#39897=CARTESIAN_POINT('Origin',(1.,0.,0.));
#39898=CARTESIAN_POINT('',(1.80411241501588E-15,-7.9602041944578E-16,6.5));
#39899=CARTESIAN_POINT('',(1.,-9.18485099360515E-16,7.5));
#39900=CARTESIAN_POINT('Origin',(1.73472347597681E-15,0.,0.));
#39901=CARTESIAN_POINT('Origin',(2.85000000000001,7.5,0.));
#39902=CARTESIAN_POINT('Origin',(4.00000000000001,7.5,0.));
#39903=CARTESIAN_POINT('Origin',(13.,8.99999999999991,0.));
#39904=CARTESIAN_POINT('Origin',(790.,7.7000000000001,0.));
#39905=CARTESIAN_POINT('Origin',(830.,6.20000000000003,0.));
#39906=CARTESIAN_POINT('Origin',(850.,0.,0.));
#39907=CARTESIAN_POINT('',(850.,2.,4.58257569495592));
#39908=CARTESIAN_POINT('Ctrl Pts',(849.000000000013,2.,5.65685424947835));
#39909=CARTESIAN_POINT('Ctrl Pts',(849.552457927857,2.,5.07088412883036));
#39910=CARTESIAN_POINT('Ctrl Pts',(850.,2.,4.58257569495594));
#39911=CARTESIAN_POINT('',(850.,-2.,4.58257569495592));
#39912=CARTESIAN_POINT('Origin',(850.,0.,0.));
#39913=CARTESIAN_POINT('Ctrl Pts',(850.000000000053,-2.,4.58257569489865));
#39914=CARTESIAN_POINT('Ctrl Pts',(849.552457927889,-2.,5.07088412879636));
#39915=CARTESIAN_POINT('Ctrl Pts',(849.000000000013,-2.,5.65685424947841));
#39916=CARTESIAN_POINT('Origin',(850.,0.,0.));
#39917=CARTESIAN_POINT('',(850.,2.,3.50000000000002));
#39918=CARTESIAN_POINT('',(850.,2.,6.00000000000002));
#39919=CARTESIAN_POINT('',(850.,-2.,3.50000000000002));
#39920=CARTESIAN_POINT('',(850.,2.,3.50000000000002));
#39921=CARTESIAN_POINT('',(850.,-2.,-6.93889390390722E-16));
#39922=CARTESIAN_POINT('Origin',(4.40872847693047E-16,6.5,0.));
#39923=CARTESIAN_POINT('Origin',(838.,2.,6.00000000000002));
#39924=CARTESIAN_POINT('',(840.,2.,3.50000000000002));
#39925=CARTESIAN_POINT('',(840.,2.,3.50000000000002));
#39926=CARTESIAN_POINT('',(838.,2.,3.50000000000002));
#39927=CARTESIAN_POINT('Origin',(838.,-2.,3.50000000000002));
#39928=CARTESIAN_POINT('',(840.,-2.,3.50000000000002));
#39929=CARTESIAN_POINT('',(838.,-2.,3.50000000000002));
#39930=CARTESIAN_POINT('',(840.,-2.,5.65685424949241));
#39931=CARTESIAN_POINT('Origin',(838.,2.,3.50000000000002));
#39932=CARTESIAN_POINT('Origin',(840.,1.30104260698261E-15,3.50000000000002));
#39933=CARTESIAN_POINT('Origin',(840.,6.93889390390719E-16,-1.20370621524202E-31));
#66654=UNCERTAINTY_MEASURE_WITH_UNIT(LENGTH_MEASURE(0.01),#66722,
'DISTANCE_ACCURACY_VALUE',
'Maximum model space distance between geometric entities at asserted c
onnectivities');
#66680=UNCERTAINTY_MEASURE_WITH_UNIT(LENGTH_MEASURE(0.01),#66722,
'DISTANCE_ACCURACY_VALUE',
'Maximum model space distance between geometric entities at asserted c
onnectivities');
#66695=(
GEOMETRIC_REPRESENTATION_CONTEXT(3)
GLOBAL_UNCERTAINTY_ASSIGNED_CONTEXT((#66654))
GLOBAL_UNIT_ASSIGNED_CONTEXT((#66722,#66724,#66725))
REPRESENTATION_CONTEXT('','3D')
);
#66721=(
GEOMETRIC_REPRESENTATION_CONTEXT(3)
GLOBAL_UNCERTAINTY_ASSIGNED_CONTEXT((#66680))
GLOBAL_UNIT_ASSIGNED_CONTEXT((#66722,#66724,#66725))
REPRESENTATION_CONTEXT('','3D')
);
#66722=(
LENGTH_UNIT()
NAMED_UNIT(*)
SI_UNIT(.MILLI.,.METRE.)
);
#66724=(
NAMED_UNIT(*)
PLANE_ANGLE_UNIT()
SI_UNIT($,.RADIAN.)
);
#66725=(
NAMED_UNIT(*)
SI_UNIT($,.STERADIAN.)
SOLID_ANGLE_UNIT()
);
#66740=SHAPE_DEFINITION_REPRESENTATION(#66792,#66904);
#66792=PRODUCT_DEFINITION_SHAPE('',$,#66945);
#66904=SHAPE_REPRESENTATION('',(#27275),#66695);
#66930=PRODUCT_DEFINITION_CONTEXT('part definition',#67052,'design');
#66945=PRODUCT_DEFINITION('Ball Screw Shaft','Ball Screw Shaft',#66985,
#66930);
#66985=PRODUCT_DEFINITION_FORMATION('',$,#67068);
#67052=APPLICATION_CONTEXT(
'Core Data for Automotive Mechanical Design Process');
#67053=PRODUCT_CONTEXT('part definition',#67052,'mechanical');
#67068=PRODUCT('Ball Screw Shaft','Ball Screw Shaft',$,(#67053));
#67095=PRESENTATION_STYLE_ASSIGNMENT((#67097));
#67097=SURFACE_STYLE_USAGE(.BOTH.,#67099);
#67099=SURFACE_SIDE_STYLE('',(#67101));
#67101=SURFACE_STYLE_FILL_AREA(#67103);
#67103=FILL_AREA_STYLE('Opaque(202,209,238)',(#67105));
#67105=FILL_AREA_STYLE_COLOUR('Opaque(202,209,238)',#67107);
#67107=COLOUR_RGB('Opaque(202,209,238)',0.792156862745098,0.819607843137255,
0.933333333333333);
ENDSEC;
END-ISO-10303-21;
